ISO-10303-21;
HEADER;
/* Generated by software containing ST-Developer
 * from STEP Tools, Inc. (www.steptools.com) 
 */

FILE_DESCRIPTION(
/* description */ ('Turntable on roller ring'),
/* implementation_level */ '2;1');

FILE_NAME(
/* name */ 'Roller tread (2).step',
/* time_stamp */ '2026-10-28T03:23:59-07:00',
/* author */ (''),
/* organization */ (''),
/* preprocessor_version */ 'ST-DEVELOPER v20.2',
/* originating_system */ 'Autodesk Translation Framework v15.17.0.0',
/* authorisation */ '');

FILE_SCHEMA (('AUTOMOTIVE_DESIGN { 1 0 10303 214 3 1 1 }'));
ENDSEC;

DATA;
#10=MECHANICAL_DESIGN_GEOMETRIC_PRESENTATION_REPRESENTATION('',(#670),#16281);
#551=SHAPE_REPRESENTATION_RELATIONSHIP('SRR','None',#16574,#606);
#606=ADVANCED_BREP_SHAPE_REPRESENTATION('',(#738),#16268);
#670=STYLED_ITEM('',(#16925),#738);
#738=MANIFOLD_SOLID_BREP('Body1',#8415);
#969=FACE_BOUND('',#2400,.T.);
#970=FACE_BOUND('',#2402,.T.);
#1221=PLANE('',#9992);
#1222=PLANE('',#9993);
#1680=FACE_OUTER_BOUND('',#2397,.T.);
#1681=FACE_OUTER_BOUND('',#2398,.T.);
#1682=FACE_OUTER_BOUND('',#2399,.T.);
#1683=FACE_OUTER_BOUND('',#2401,.T.);
#2397=EDGE_LOOP('',(#7385,#7386,#7387,#7388));
#2398=EDGE_LOOP('',(#7389,#7390,#7391,#7392));
#2399=EDGE_LOOP('',(#7393));
#2400=EDGE_LOOP('',(#7394));
#2401=EDGE_LOOP('',(#7395));
#2402=EDGE_LOOP('',(#7396));
#2948=LINE('',#15446,#3431);
#2949=LINE('',#15452,#3432);
#3431=VECTOR('',#12551,1.5);
#3432=VECTOR('',#12558,2.);
#3853=CIRCLE('',#9987,1.5);
#3854=CIRCLE('',#9988,1.5);
#3855=CIRCLE('',#9990,2.);
#3856=CIRCLE('',#9991,2.);
#4529=VERTEX_POINT('',#15443);
#4530=VERTEX_POINT('',#15445);
#4531=VERTEX_POINT('',#15449);
#4532=VERTEX_POINT('',#15451);
#5503=EDGE_CURVE('',#4529,#4529,#3853,.T.);
#5504=EDGE_CURVE('',#4529,#4530,#2948,.T.);
#5505=EDGE_CURVE('',#4530,#4530,#3854,.T.);
#5506=EDGE_CURVE('',#4531,#4531,#3855,.T.);
#5507=EDGE_CURVE('',#4531,#4532,#2949,.T.);
#5508=EDGE_CURVE('',#4532,#4532,#3856,.T.);
#7385=ORIENTED_EDGE('',*,*,#5503,.F.);
#7386=ORIENTED_EDGE('',*,*,#5504,.T.);
#7387=ORIENTED_EDGE('',*,*,#5505,.T.);
#7388=ORIENTED_EDGE('',*,*,#5504,.F.);
#7389=ORIENTED_EDGE('',*,*,#5506,.F.);
#7390=ORIENTED_EDGE('',*,*,#5507,.T.);
#7391=ORIENTED_EDGE('',*,*,#5508,.T.);
#7392=ORIENTED_EDGE('',*,*,#5507,.F.);
#7393=ORIENTED_EDGE('',*,*,#5506,.T.);
#7394=ORIENTED_EDGE('',*,*,#5503,.T.);
#7395=ORIENTED_EDGE('',*,*,#5508,.F.);
#7396=ORIENTED_EDGE('',*,*,#5505,.F.);
#7829=CYLINDRICAL_SURFACE('',#9986,1.5);
#7830=CYLINDRICAL_SURFACE('',#9989,2.);
#8283=ADVANCED_FACE('',(#1680),#7829,.F.);
#8284=ADVANCED_FACE('',(#1681),#7830,.T.);
#8285=ADVANCED_FACE('',(#1682,#969),#1221,.T.);
#8286=ADVANCED_FACE('',(#1683,#970),#1222,.F.);
#8415=CLOSED_SHELL('',(#8283,#8284,#8285,#8286));
#9985=AXIS2_PLACEMENT_3D('',#15441,#12545,#12546);
#9986=AXIS2_PLACEMENT_3D('',#15442,#12547,#12548);
#9987=AXIS2_PLACEMENT_3D('',#15444,#12549,#12550);
#9988=AXIS2_PLACEMENT_3D('',#15447,#12552,#12553);
#9989=AXIS2_PLACEMENT_3D('',#15448,#12554,#12555);
#9990=AXIS2_PLACEMENT_3D('',#15450,#12556,#12557);
#9991=AXIS2_PLACEMENT_3D('',#15453,#12559,#12560);
#9992=AXIS2_PLACEMENT_3D('',#15454,#12561,#12562);
#9993=AXIS2_PLACEMENT_3D('',#15455,#12563,#12564);
#12545=DIRECTION('axis',(0.,0.,1.));
#12546=DIRECTION('refdir',(1.,0.,0.));
#12547=DIRECTION('center_axis',(0.,1.,0.));
#12548=DIRECTION('ref_axis',(1.,0.,0.));
#12549=DIRECTION('center_axis',(0.,-1.,0.));
#12550=DIRECTION('ref_axis',(1.,0.,0.));
#12551=DIRECTION('',(0.,-1.,0.));
#12552=DIRECTION('center_axis',(0.,-1.,0.));
#12553=DIRECTION('ref_axis',(1.,0.,0.));
#12554=DIRECTION('center_axis',(0.,1.,0.));
#12555=DIRECTION('ref_axis',(1.,0.,0.));
#12556=DIRECTION('center_axis',(0.,1.,0.));
#12557=DIRECTION('ref_axis',(1.,0.,0.));
#12558=DIRECTION('',(0.,-1.,0.));
#12559=DIRECTION('center_axis',(0.,1.,0.));
#12560=DIRECTION('ref_axis',(1.,0.,0.));
#12561=DIRECTION('center_axis',(0.,1.,0.));
#12562=DIRECTION('ref_axis',(1.,0.,0.));
#12563=DIRECTION('center_axis',(0.,1.,0.));
#12564=DIRECTION('ref_axis',(1.,0.,0.));
#15441=CARTESIAN_POINT('',(0.,0.,0.));
#15442=CARTESIAN_POINT('Origin',(0.,14.35,3.5));
#15443=CARTESIAN_POINT('',(-1.5,15.65,3.5));
#15444=CARTESIAN_POINT('Origin',(0.,15.65,3.5));
#15445=CARTESIAN_POINT('',(-1.5,14.35,3.5));
#15446=CARTESIAN_POINT('',(-1.5,14.35,3.5));
#15447=CARTESIAN_POINT('Origin',(0.,14.35,3.5));
#15448=CARTESIAN_POINT('Origin',(0.,14.35,3.5));
#15449=CARTESIAN_POINT('',(-2.,15.65,3.5));
#15450=CARTESIAN_POINT('Origin',(0.,15.65,3.5));
#15451=CARTESIAN_POINT('',(-2.,14.35,3.5));
#15452=CARTESIAN_POINT('',(-2.,14.35,3.5));
#15453=CARTESIAN_POINT('Origin',(0.,14.35,3.5));
#15454=CARTESIAN_POINT('Origin',(0.,15.65,3.5));
#15455=CARTESIAN_POINT('Origin',(0.,14.35,3.5));
#16199=UNCERTAINTY_MEASURE_WITH_UNIT(LENGTH_MEASURE(0.001),#16282,
'DISTANCE_ACCURACY_VALUE',
'Maximum model space distance between geometric entities at asserted c
onnectivities');
#16212=UNCERTAINTY_MEASURE_WITH_UNIT(LENGTH_MEASURE(0.001),#16282,
'DISTANCE_ACCURACY_VALUE',
'Maximum model space distance between geometric entities at asserted c
onnectivities');
#16268=(
GEOMETRIC_REPRESENTATION_CONTEXT(3)
GLOBAL_UNCERTAINTY_ASSIGNED_CONTEXT((#16199))
GLOBAL_UNIT_ASSIGNED_CONTEXT((#16282,#16284,#16285))
REPRESENTATION_CONTEXT('','3D')
);
#16281=(
GEOMETRIC_REPRESENTATION_CONTEXT(3)
GLOBAL_UNCERTAINTY_ASSIGNED_CONTEXT((#16212))
GLOBAL_UNIT_ASSIGNED_CONTEXT((#16282,#16284,#16285))
REPRESENTATION_CONTEXT('','3D')
);
#16282=(
LENGTH_UNIT()
NAMED_UNIT(*)
SI_UNIT(.CENTI.,.METRE.)
);
#16284=(
NAMED_UNIT(*)
PLANE_ANGLE_UNIT()
SI_UNIT($,.RADIAN.)
);
#16285=(
NAMED_UNIT(*)
SI_UNIT($,.STERADIAN.)
SOLID_ANGLE_UNIT()
);
#16341=SHAPE_DEFINITION_REPRESENTATION(#16475,#16574);
#16475=PRODUCT_DEFINITION_SHAPE('',$,#16643);
#16574=SHAPE_REPRESENTATION('',(#9985),#16268);
#16587=PRODUCT_DEFINITION_CONTEXT('part definition',#16793,'design');
#16643=PRODUCT_DEFINITION('Roller tread (2)','Roller tread (2)',#16711,#16587);
#16711=PRODUCT_DEFINITION_FORMATION('',$,#16850);
#16793=APPLICATION_CONTEXT(
'Core Data for Automotive Mechanical Design Process');
#16794=PRODUCT_CONTEXT('part definition',#16793,'mechanical');
#16850=PRODUCT('Roller tread (2)','Roller tread (2)','Roller tread (2)',(#16794));
#16919=COLOUR_RGB('Sky Blue',0.24,0.69,0.87);
#16920=FILL_AREA_STYLE_COLOUR('',#16919);
#16921=FILL_AREA_STYLE('',(#16920));
#16922=SURFACE_STYLE_FILL_AREA(#16921);
#16923=SURFACE_SIDE_STYLE('',(#16922));
#16924=SURFACE_STYLE_USAGE(.BOTH.,#16923);
#16925=PRESENTATION_STYLE_ASSIGNMENT((#16924));
ENDSEC;
END-ISO-10303-21;
